ISO-10303-21;
HEADER;
/* Generated by software containing ST-Developer
 * from STEP Tools, Inc. (www.steptools.com) 
 */

FILE_DESCRIPTION(
/* description */ ('Torque wrench calibration arm'),
/* implementation_level */ '2;1');

FILE_NAME(
/* name */ 'Inner ring (1).step',
/* time_stamp */ '2026-10-28T03:24:52-07:00',
/* author */ (''),
/* organization */ (''),
/* preprocessor_version */ 'ST-DEVELOPER v20.2',
/* originating_system */ 'Autodesk Translation Framework v15.17.0.0',
/* authorisation */ '');

FILE_SCHEMA (('AUTOMOTIVE_DESIGN { 1 0 10303 214 3 1 1 }'));
ENDSEC;

DATA;
#10=MECHANICAL_DESIGN_GEOMETRIC_PRESENTATION_REPRESENTATION('',(#458),#12783);
#341=CONICAL_SURFACE('',#7550,0.53,0.785398163397448);
#342=CONICAL_SURFACE('',#7557,0.53,0.785398163397448);
#350=TOROIDAL_SURFACE('',#7539,1.,0.247676);
#375=SHAPE_REPRESENTATION_RELATIONSHIP('SRR','None',#12959,#412);
#412=ADVANCED_BREP_SHAPE_REPRESENTATION('',(#510),#12768);
#458=STYLED_ITEM('',(#13212),#510);
#510=MANIFOLD_SOLID_BREP('Body1',#6529);
#622=FACE_BOUND('',#1650,.T.);
#623=FACE_BOUND('',#1653,.T.);
#821=PLANE('',#7552);
#822=PLANE('',#7555);
#1159=FACE_OUTER_BOUND('',#1645,.T.);
#1160=FACE_OUTER_BOUND('',#1646,.T.);
#1161=FACE_OUTER_BOUND('',#1647,.T.);
#1162=FACE_OUTER_BOUND('',#1648,.T.);
#1163=FACE_OUTER_BOUND('',#1649,.T.);
#1164=FACE_OUTER_BOUND('',#1651,.T.);
#1165=FACE_OUTER_BOUND('',#1652,.T.);
#1166=FACE_OUTER_BOUND('',#1654,.T.);
#1645=EDGE_LOOP('',(#5559,#5560,#5561,#5562,#5563,#5564));
#1646=EDGE_LOOP('',(#5565,#5566,#5567,#5568,#5569));
#1647=EDGE_LOOP('',(#5570,#5571,#5572,#5573));
#1648=EDGE_LOOP('',(#5574,#5575,#5576,#5577));
#1649=EDGE_LOOP('',(#5578));
#1650=EDGE_LOOP('',(#5579));
#1651=EDGE_LOOP('',(#5580,#5581,#5582,#5583,#5584));
#1652=EDGE_LOOP('',(#5585));
#1653=EDGE_LOOP('',(#5586));
#1654=EDGE_LOOP('',(#5587,#5588,#5589,#5590));
#2120=LINE('',#11849,#2535);
#2121=LINE('',#11855,#2536);
#2122=LINE('',#11859,#2537);
#2123=LINE('',#11865,#2538);
#2124=LINE('',#11870,#2539);
#2535=VECTOR('',#9316,0.976185);
#2536=VECTOR('',#9323,0.5);
#2537=VECTOR('',#9328,0.53);
#2538=VECTOR('',#9337,0.976185);
#2539=VECTOR('',#9344,0.53);
#2856=CIRCLE('',#7540,0.976185);
#2857=CIRCLE('',#7541,0.976185);
#2858=CIRCLE('',#7542,0.247676);
#2859=CIRCLE('',#7543,0.976185);
#2860=CIRCLE('',#7544,0.976185);
#2861=CIRCLE('',#7546,0.976185);
#2862=CIRCLE('',#7548,0.5);
#2863=CIRCLE('',#7549,0.5);
#2864=CIRCLE('',#7551,0.56);
#2865=CIRCLE('',#7554,0.976185);
#2866=CIRCLE('',#7556,0.56);
#3382=VERTEX_POINT('',#11838);
#3383=VERTEX_POINT('',#11839);
#3384=VERTEX_POINT('',#11842);
#3385=VERTEX_POINT('',#11844);
#3386=VERTEX_POINT('',#11848);
#3387=VERTEX_POINT('',#11852);
#3388=VERTEX_POINT('',#11854);
#3389=VERTEX_POINT('',#11858);
#3390=VERTEX_POINT('',#11863);
#3391=VERTEX_POINT('',#11867);
#4137=EDGE_CURVE('',#3382,#3383,#2856,.T.);
#4138=EDGE_CURVE('',#3383,#3382,#2857,.T.);
#4139=EDGE_CURVE('',#3383,#3384,#2858,.T.);
#4140=EDGE_CURVE('',#3385,#3384,#2859,.T.);
#4141=EDGE_CURVE('',#3384,#3385,#2860,.T.);
#4142=EDGE_CURVE('',#3385,#3386,#2120,.T.);
#4143=EDGE_CURVE('',#3386,#3386,#2861,.T.);
#4144=EDGE_CURVE('',#3387,#3387,#2862,.T.);
#4145=EDGE_CURVE('',#3387,#3388,#2121,.T.);
#4146=EDGE_CURVE('',#3388,#3388,#2863,.T.);
#4147=EDGE_CURVE('',#3388,#3389,#2122,.T.);
#4148=EDGE_CURVE('',#3389,#3389,#2864,.T.);
#4149=EDGE_CURVE('',#3390,#3390,#2865,.T.);
#4150=EDGE_CURVE('',#3390,#3382,#2123,.T.);
#4151=EDGE_CURVE('',#3391,#3391,#2866,.T.);
#4152=EDGE_CURVE('',#3391,#3387,#2124,.T.);
#5559=ORIENTED_EDGE('',*,*,#4137,.F.);
#5560=ORIENTED_EDGE('',*,*,#4138,.F.);
#5561=ORIENTED_EDGE('',*,*,#4139,.T.);
#5562=ORIENTED_EDGE('',*,*,#4140,.F.);
#5563=ORIENTED_EDGE('',*,*,#4141,.F.);
#5564=ORIENTED_EDGE('',*,*,#4139,.F.);
#5565=ORIENTED_EDGE('',*,*,#4140,.T.);
#5566=ORIENTED_EDGE('',*,*,#4141,.T.);
#5567=ORIENTED_EDGE('',*,*,#4142,.T.);
#5568=ORIENTED_EDGE('',*,*,#4143,.T.);
#5569=ORIENTED_EDGE('',*,*,#4142,.F.);
#5570=ORIENTED_EDGE('',*,*,#4144,.T.);
#5571=ORIENTED_EDGE('',*,*,#4145,.T.);
#5572=ORIENTED_EDGE('',*,*,#4146,.F.);
#5573=ORIENTED_EDGE('',*,*,#4145,.F.);
#5574=ORIENTED_EDGE('',*,*,#4146,.T.);
#5575=ORIENTED_EDGE('',*,*,#4147,.T.);
#5576=ORIENTED_EDGE('',*,*,#4148,.F.);
#5577=ORIENTED_EDGE('',*,*,#4147,.F.);
#5578=ORIENTED_EDGE('',*,*,#4143,.F.);
#5579=ORIENTED_EDGE('',*,*,#4148,.T.);
#5580=ORIENTED_EDGE('',*,*,#4149,.F.);
#5581=ORIENTED_EDGE('',*,*,#4150,.T.);
#5582=ORIENTED_EDGE('',*,*,#4137,.T.);
#5583=ORIENTED_EDGE('',*,*,#4138,.T.);
#5584=ORIENTED_EDGE('',*,*,#4150,.F.);
#5585=ORIENTED_EDGE('',*,*,#4149,.T.);
#5586=ORIENTED_EDGE('',*,*,#4151,.F.);
#5587=ORIENTED_EDGE('',*,*,#4151,.T.);
#5588=ORIENTED_EDGE('',*,*,#4152,.T.);
#5589=ORIENTED_EDGE('',*,*,#4144,.F.);
#5590=ORIENTED_EDGE('',*,*,#4152,.F.);
#6068=CYLINDRICAL_SURFACE('',#7545,0.976185);
#6069=CYLINDRICAL_SURFACE('',#7547,0.5);
#6070=CYLINDRICAL_SURFACE('',#7553,0.976185);
#6384=ADVANCED_FACE('',(#1159),#350,.F.);
#6385=ADVANCED_FACE('',(#1160),#6068,.T.);
#6386=ADVANCED_FACE('',(#1161),#6069,.F.);
#6387=ADVANCED_FACE('',(#1162),#341,.F.);
#6388=ADVANCED_FACE('',(#1163,#622),#821,.T.);
#6389=ADVANCED_FACE('',(#1164),#6070,.T.);
#6390=ADVANCED_FACE('',(#1165,#623),#822,.T.);
#6391=ADVANCED_FACE('',(#1166),#342,.F.);
#6529=CLOSED_SHELL('',(#6384,#6385,#6386,#6387,#6388,#6389,#6390,#6391));
#7538=AXIS2_PLACEMENT_3D('',#11836,#9300,#9301);
#7539=AXIS2_PLACEMENT_3D('',#11837,#9302,#9303);
#7540=AXIS2_PLACEMENT_3D('',#11840,#9304,#9305);
#7541=AXIS2_PLACEMENT_3D('',#11841,#9306,#9307);
#7542=AXIS2_PLACEMENT_3D('',#11843,#9308,#9309);
#7543=AXIS2_PLACEMENT_3D('',#11845,#9310,#9311);
#7544=AXIS2_PLACEMENT_3D('',#11846,#9312,#9313);
#7545=AXIS2_PLACEMENT_3D('',#11847,#9314,#9315);
#7546=AXIS2_PLACEMENT_3D('',#11850,#9317,#9318);
#7547=AXIS2_PLACEMENT_3D('',#11851,#9319,#9320);
#7548=AXIS2_PLACEMENT_3D('',#11853,#9321,#9322);
#7549=AXIS2_PLACEMENT_3D('',#11856,#9324,#9325);
#7550=AXIS2_PLACEMENT_3D('',#11857,#9326,#9327);
#7551=AXIS2_PLACEMENT_3D('',#11860,#9329,#9330);
#7552=AXIS2_PLACEMENT_3D('',#11861,#9331,#9332);
#7553=AXIS2_PLACEMENT_3D('',#11862,#9333,#9334);
#7554=AXIS2_PLACEMENT_3D('',#11864,#9335,#9336);
#7555=AXIS2_PLACEMENT_3D('',#11866,#9338,#9339);
#7556=AXIS2_PLACEMENT_3D('',#11868,#9340,#9341);
#7557=AXIS2_PLACEMENT_3D('',#11869,#9342,#9343);
#9300=DIRECTION('axis',(0.,0.,1.));
#9301=DIRECTION('refdir',(1.,0.,0.));
#9302=DIRECTION('center_axis',(0.,-1.,0.));
#9303=DIRECTION('ref_axis',(0.,0.,-1.));
#9304=DIRECTION('center_axis',(0.,-1.,0.));
#9305=DIRECTION('ref_axis',(1.,0.,0.));
#9306=DIRECTION('center_axis',(0.,-1.,0.));
#9307=DIRECTION('ref_axis',(1.,0.,0.));
#9308=DIRECTION('center_axis',(1.,0.,1.22464679914735E-16));
#9309=DIRECTION('ref_axis',(-1.22464679914735E-16,0.,1.));
#9310=DIRECTION('center_axis',(0.,1.,0.));
#9311=DIRECTION('ref_axis',(1.,0.,0.));
#9312=DIRECTION('center_axis',(0.,1.,0.));
#9313=DIRECTION('ref_axis',(1.,0.,0.));
#9314=DIRECTION('center_axis',(0.,-1.,0.));
#9315=DIRECTION('ref_axis',(1.,0.,0.));
#9316=DIRECTION('',(0.,1.,0.));
#9317=DIRECTION('center_axis',(0.,-1.,0.));
#9318=DIRECTION('ref_axis',(1.,0.,0.));
#9319=DIRECTION('center_axis',(0.,-1.,0.));
#9320=DIRECTION('ref_axis',(1.,0.,0.));
#9321=DIRECTION('center_axis',(0.,-1.,0.));
#9322=DIRECTION('ref_axis',(1.,0.,0.));
#9323=DIRECTION('',(0.,1.,0.));
#9324=DIRECTION('center_axis',(0.,-1.,0.));
#9325=DIRECTION('ref_axis',(1.,0.,0.));
#9326=DIRECTION('center_axis',(0.,1.,0.));
#9327=DIRECTION('ref_axis',(1.,0.,0.));
#9328=DIRECTION('',(-0.707106781186547,0.707106781186548,-8.65956056235493E-17));
#9329=DIRECTION('center_axis',(0.,-1.,0.));
#9330=DIRECTION('ref_axis',(1.,0.,0.));
#9331=DIRECTION('center_axis',(0.,1.,0.));
#9332=DIRECTION('ref_axis',(0.,0.,1.));
#9333=DIRECTION('center_axis',(0.,-1.,0.));
#9334=DIRECTION('ref_axis',(1.,0.,0.));
#9335=DIRECTION('center_axis',(0.,-1.,0.));
#9336=DIRECTION('ref_axis',(1.,0.,0.));
#9337=DIRECTION('',(0.,1.,0.));
#9338=DIRECTION('center_axis',(0.,-1.,0.));
#9339=DIRECTION('ref_axis',(0.,0.,-1.));
#9340=DIRECTION('center_axis',(0.,-1.,0.));
#9341=DIRECTION('ref_axis',(1.,0.,0.));
#9342=DIRECTION('center_axis',(0.,-1.,0.));
#9343=DIRECTION('ref_axis',(1.,0.,0.));
#9344=DIRECTION('',(0.707106781186547,0.707106781186548,8.65956056235493E-17));
#11836=CARTESIAN_POINT('',(0.,0.,0.));
#11837=CARTESIAN_POINT('Origin',(0.,0.,0.));
#11838=CARTESIAN_POINT('',(-0.976185,-0.246528389340863,-1.19548183562566E-16));
#11839=CARTESIAN_POINT('',(-1.19548183562566E-16,-0.246528389340863,0.976185));
#11840=CARTESIAN_POINT('Origin',(0.,-0.246528389340863,0.));
#11841=CARTESIAN_POINT('Origin',(0.,-0.246528389340863,0.));
#11842=CARTESIAN_POINT('',(-1.19548183562566E-16,0.246528389340863,0.976185));
#11843=CARTESIAN_POINT('Origin',(-1.22464679914735E-16,0.,1.));
#11844=CARTESIAN_POINT('',(-0.976185,0.246528389340863,1.19548183562566E-16));
#11845=CARTESIAN_POINT('Origin',(0.,0.246528389340863,0.));
#11846=CARTESIAN_POINT('Origin',(0.,0.246528389340863,0.));
#11847=CARTESIAN_POINT('Origin',(0.,0.,0.));
#11848=CARTESIAN_POINT('',(-0.976185,0.45,-1.19548183562566E-16));
#11849=CARTESIAN_POINT('',(-0.976185,0.,-1.19548183562566E-16));
#11850=CARTESIAN_POINT('Origin',(0.,0.45,0.));
#11851=CARTESIAN_POINT('Origin',(0.,0.,0.));
#11852=CARTESIAN_POINT('',(-0.5,-0.39,-6.12323399573677E-17));
#11853=CARTESIAN_POINT('Origin',(0.,-0.39,0.));
#11854=CARTESIAN_POINT('',(-0.5,0.39,-6.12323399573677E-17));
#11855=CARTESIAN_POINT('',(-0.5,0.,-6.12323399573677E-17));
#11856=CARTESIAN_POINT('Origin',(0.,0.39,0.));
#11857=CARTESIAN_POINT('Origin',(0.,0.42,0.));
#11858=CARTESIAN_POINT('',(-0.56,0.45,-6.85802207522518E-17));
#11859=CARTESIAN_POINT('',(-0.53,0.42,-6.49062803548097E-17));
#11860=CARTESIAN_POINT('Origin',(0.,0.45,0.));
#11861=CARTESIAN_POINT('Origin',(0.976185,0.45,0.));
#11862=CARTESIAN_POINT('Origin',(0.,0.,0.));
#11863=CARTESIAN_POINT('',(-0.976185,-0.45,-1.19548183562566E-16));
#11864=CARTESIAN_POINT('Origin',(0.,-0.45,0.));
#11865=CARTESIAN_POINT('',(-0.976185,0.,-1.19548183562566E-16));
#11866=CARTESIAN_POINT('Origin',(0.56,-0.45,0.));
#11867=CARTESIAN_POINT('',(-0.56,-0.45,-6.85802207522518E-17));
#11868=CARTESIAN_POINT('Origin',(0.,-0.45,0.));
#11869=CARTESIAN_POINT('Origin',(0.,-0.42,0.));
#11870=CARTESIAN_POINT('',(-0.53,-0.42,-6.49062803548097E-17));
#12724=UNCERTAINTY_MEASURE_WITH_UNIT(LENGTH_MEASURE(0.001),#12784,
'DISTANCE_ACCURACY_VALUE',
'Maximum model space distance between geometric entities at asserted c
onnectivities');
#12739=UNCERTAINTY_MEASURE_WITH_UNIT(LENGTH_MEASURE(0.001),#12784,
'DISTANCE_ACCURACY_VALUE',
'Maximum model space distance between geometric entities at asserted c
onnectivities');
#12768=(
GEOMETRIC_REPRESENTATION_CONTEXT(3)
GLOBAL_UNCERTAINTY_ASSIGNED_CONTEXT((#12724))
GLOBAL_UNIT_ASSIGNED_CONTEXT((#12784,#12786,#12787))
REPRESENTATION_CONTEXT('','3D')
);
#12783=(
GEOMETRIC_REPRESENTATION_CONTEXT(3)
GLOBAL_UNCERTAINTY_ASSIGNED_CONTEXT((#12739))
GLOBAL_UNIT_ASSIGNED_CONTEXT((#12784,#12786,#12787))
REPRESENTATION_CONTEXT('','3D')
);
#12784=(
LENGTH_UNIT()
NAMED_UNIT(*)
SI_UNIT(.CENTI.,.METRE.)
);
#12786=(
NAMED_UNIT(*)
PLANE_ANGLE_UNIT()
SI_UNIT($,.RADIAN.)
);
#12787=(
NAMED_UNIT(*)
SI_UNIT($,.STERADIAN.)
SOLID_ANGLE_UNIT()
);
#12816=SHAPE_DEFINITION_REPRESENTATION(#12885,#12959);
#12885=PRODUCT_DEFINITION_SHAPE('',$,#13003);
#12959=SHAPE_REPRESENTATION('',(#7538),#12768);
#12974=PRODUCT_DEFINITION_CONTEXT('part definition',#13105,'design');
#13003=PRODUCT_DEFINITION('Inner ring (1)','Inner ring (1)',#13046,#12974);
#13046=PRODUCT_DEFINITION_FORMATION('',$,#13135);
#13105=APPLICATION_CONTEXT(
'Core Data for Automotive Mechanical Design Process');
#13106=PRODUCT_CONTEXT('part definition',#13105,'mechanical');
#13135=PRODUCT('Inner ring (1)','Inner ring (1)','Inner ring (1)',(#13106));
#13206=COLOUR_RGB('Grey',0.48,0.52,0.57);
#13207=FILL_AREA_STYLE_COLOUR('',#13206);
#13208=FILL_AREA_STYLE('',(#13207));
#13209=SURFACE_STYLE_FILL_AREA(#13208);
#13210=SURFACE_SIDE_STYLE('',(#13209));
#13211=SURFACE_STYLE_USAGE(.BOTH.,#13210);
#13212=PRESENTATION_STYLE_ASSIGNMENT((#13211));
ENDSEC;
END-ISO-10303-21;
